ISO-10303-21;
HEADER;
/* Generated by software containing ST-Developer
 * from STEP Tools, Inc. (www.steptools.com) 
 */

FILE_DESCRIPTION(
/* description */ ('Four-bar parallelogram arm'),
/* implementation_level */ '2;1');

FILE_NAME(
/* name */ 'M4x10 Cap Screw.step',
/* time_stamp */ '2026-10-28T03:24:55-07:00',
/* author */ (''),
/* organization */ (''),
/* preprocessor_version */ 'ST-DEVELOPER v20.2',
/* originating_system */ 'Autodesk Translation Framework v15.17.0.0',
/* authorisation */ '');

FILE_SCHEMA (('AUTOMOTIVE_DESIGN { 1 0 10303 214 3 1 1 }'));
ENDSEC;

DATA;
#10=MECHANICAL_DESIGN_GEOMETRIC_PRESENTATION_REPRESENTATION('',(#667),#14512);
#484=CONICAL_SURFACE('',#8653,0.325,0.785398163397448);
#485=CONICAL_SURFACE('',#8657,0.335,0.785398163397448);
#486=CONICAL_SURFACE('',#8661,0.21,0.463647609000806);
#492=ORIENTED_CLOSED_SHELL('',*,#7372,.F.);
#495=BREP_WITH_VOIDS('Body1',#7373,(#492));
#559=SHAPE_REPRESENTATION_RELATIONSHIP('SRR','None',#14783,#609);
#609=ADVANCED_BREP_SHAPE_REPRESENTATION('',(#495),#14498);
#667=STYLED_ITEM('',(#15094),#495);
#946=FACE_BOUND('',#2156,.T.);
#1144=PLANE('',#8641);
#1145=PLANE('',#8642);
#1146=PLANE('',#8643);
#1147=PLANE('',#8644);
#1148=PLANE('',#8645);
#1149=PLANE('',#8646);
#1150=PLANE('',#8647);
#1151=PLANE('',#8648);
#1152=PLANE('',#8649);
#1153=PLANE('',#8651);
#1154=PLANE('',#8659);
#1511=FACE_OUTER_BOUND('',#2142,.T.);
#1512=FACE_OUTER_BOUND('',#2143,.T.);
#1513=FACE_OUTER_BOUND('',#2144,.T.);
#1514=FACE_OUTER_BOUND('',#2145,.T.);
#1515=FACE_OUTER_BOUND('',#2146,.T.);
#1516=FACE_OUTER_BOUND('',#2147,.T.);
#1517=FACE_OUTER_BOUND('',#2148,.T.);
#1518=FACE_OUTER_BOUND('',#2149,.T.);
#1519=FACE_OUTER_BOUND('',#2150,.T.);
#1520=FACE_OUTER_BOUND('',#2151,.T.);
#1521=FACE_OUTER_BOUND('',#2152,.T.);
#1522=FACE_OUTER_BOUND('',#2153,.T.);
#1523=FACE_OUTER_BOUND('',#2154,.T.);
#1524=FACE_OUTER_BOUND('',#2155,.T.);
#1525=FACE_OUTER_BOUND('',#2157,.T.);
#1526=FACE_OUTER_BOUND('',#2158,.T.);
#2142=EDGE_LOOP('',(#6296,#6297,#6298,#6299));
#2143=EDGE_LOOP('',(#6300,#6301,#6302,#6303));
#2144=EDGE_LOOP('',(#6304,#6305,#6306,#6307));
#2145=EDGE_LOOP('',(#6308,#6309,#6310,#6311));
#2146=EDGE_LOOP('',(#6312,#6313,#6314,#6315));
#2147=EDGE_LOOP('',(#6316,#6317,#6318,#6319));
#2148=EDGE_LOOP('',(#6320,#6321,#6322,#6323,#6324,#6325));
#2149=EDGE_LOOP('',(#6326,#6327,#6328,#6329,#6330,#6331));
#2150=EDGE_LOOP('',(#6332));
#2151=EDGE_LOOP('',(#6333));
#2152=EDGE_LOOP('',(#6334,#6335,#6336,#6337));
#2153=EDGE_LOOP('',(#6338,#6339,#6340,#6341));
#2154=EDGE_LOOP('',(#6342,#6343,#6344,#6345));
#2155=EDGE_LOOP('',(#6346));
#2156=EDGE_LOOP('',(#6347));
#2157=EDGE_LOOP('',(#6348,#6349,#6350,#6351));
#2158=EDGE_LOOP('',(#6352,#6353,#6354,#6355));
#2596=LINE('',#13826,#2990);
#2597=LINE('',#13828,#2991);
#2598=LINE('',#13830,#2992);
#2599=LINE('',#13831,#2993);
#2600=LINE('',#13834,#2994);
#2601=LINE('',#13836,#2995);
#2602=LINE('',#13837,#2996);
#2603=LINE('',#13840,#2997);
#2604=LINE('',#13842,#2998);
#2605=LINE('',#13843,#2999);
#2606=LINE('',#13846,#3000);
#2607=LINE('',#13848,#3001);
#2608=LINE('',#13849,#3002);
#2609=LINE('',#13852,#3003);
#2610=LINE('',#13854,#3004);
#2611=LINE('',#13855,#3005);
#2612=LINE('',#13857,#3006);
#2613=LINE('',#13858,#3007);
#2614=LINE('',#13870,#3008);
#2615=LINE('',#13874,#3009);
#2616=LINE('',#13878,#3010);
#2617=LINE('',#13885,#3011);
#2618=LINE('',#13887,#3012);
#2990=VECTOR('',#10662,1.);
#2991=VECTOR('',#10663,1.);
#2992=VECTOR('',#10664,1.);
#2993=VECTOR('',#10665,1.);
#2994=VECTOR('',#10668,1.);
#2995=VECTOR('',#10669,1.);
#2996=VECTOR('',#10670,1.);
#2997=VECTOR('',#10673,1.);
#2998=VECTOR('',#10674,1.);
#2999=VECTOR('',#10675,1.);
#3000=VECTOR('',#10678,1.);
#3001=VECTOR('',#10679,1.);
#3002=VECTOR('',#10680,1.);
#3003=VECTOR('',#10683,1.);
#3004=VECTOR('',#10684,1.);
#3005=VECTOR('',#10685,1.);
#3006=VECTOR('',#10688,1.);
#3007=VECTOR('',#10689,1.);
#3008=VECTOR('',#10706,0.325);
#3009=VECTOR('',#10711,0.35);
#3010=VECTOR('',#10716,0.335);
#3011=VECTOR('',#10725,0.21);
#3012=VECTOR('',#10728,0.2);
#3446=CIRCLE('',#8650,0.1954);
#3447=CIRCLE('',#8652,0.3);
#3448=CIRCLE('',#8654,0.35);
#3449=CIRCLE('',#8656,0.35);
#3450=CIRCLE('',#8658,0.32);
#3451=CIRCLE('',#8660,0.22);
#3452=CIRCLE('',#8662,0.1954);
#3988=VERTEX_POINT('',#13824);
#3989=VERTEX_POINT('',#13825);
#3990=VERTEX_POINT('',#13827);
#3991=VERTEX_POINT('',#13829);
#3992=VERTEX_POINT('',#13833);
#3993=VERTEX_POINT('',#13835);
#3994=VERTEX_POINT('',#13839);
#3995=VERTEX_POINT('',#13841);
#3996=VERTEX_POINT('',#13845);
#3997=VERTEX_POINT('',#13847);
#3998=VERTEX_POINT('',#13851);
#3999=VERTEX_POINT('',#13853);
#4000=VERTEX_POINT('',#13862);
#4001=VERTEX_POINT('',#13865);
#4002=VERTEX_POINT('',#13868);
#4003=VERTEX_POINT('',#13872);
#4004=VERTEX_POINT('',#13876);
#4005=VERTEX_POINT('',#13880);
#4006=VERTEX_POINT('',#13883);
#4779=EDGE_CURVE('',#3988,#3989,#2596,.T.);
#4780=EDGE_CURVE('',#3989,#3990,#2597,.T.);
#4781=EDGE_CURVE('',#3990,#3991,#2598,.T.);
#4782=EDGE_CURVE('',#3988,#3991,#2599,.T.);
#4783=EDGE_CURVE('',#3989,#3992,#2600,.T.);
#4784=EDGE_CURVE('',#3992,#3993,#2601,.T.);
#4785=EDGE_CURVE('',#3993,#3990,#2602,.T.);
#4786=EDGE_CURVE('',#3992,#3994,#2603,.T.);
#4787=EDGE_CURVE('',#3994,#3995,#2604,.T.);
#4788=EDGE_CURVE('',#3995,#3993,#2605,.T.);
#4789=EDGE_CURVE('',#3994,#3996,#2606,.T.);
#4790=EDGE_CURVE('',#3996,#3997,#2607,.T.);
#4791=EDGE_CURVE('',#3997,#3995,#2608,.T.);
#4792=EDGE_CURVE('',#3996,#3998,#2609,.T.);
#4793=EDGE_CURVE('',#3998,#3999,#2610,.T.);
#4794=EDGE_CURVE('',#3999,#3997,#2611,.T.);
#4795=EDGE_CURVE('',#3998,#3988,#2612,.T.);
#4796=EDGE_CURVE('',#3991,#3999,#2613,.T.);
#4797=EDGE_CURVE('',#4000,#4000,#3446,.T.);
#4798=EDGE_CURVE('',#4001,#4001,#3447,.T.);
#4799=EDGE_CURVE('',#4002,#4002,#3448,.T.);
#4800=EDGE_CURVE('',#4002,#4001,#2614,.T.);
#4801=EDGE_CURVE('',#4003,#4003,#3449,.T.);
#4802=EDGE_CURVE('',#4003,#4002,#2615,.T.);
#4803=EDGE_CURVE('',#4004,#4004,#3450,.T.);
#4804=EDGE_CURVE('',#4004,#4003,#2616,.T.);
#4805=EDGE_CURVE('',#4005,#4005,#3451,.T.);
#4806=EDGE_CURVE('',#4006,#4006,#3452,.F.);
#4807=EDGE_CURVE('',#4006,#4005,#2617,.T.);
#4808=EDGE_CURVE('',#4000,#4006,#2618,.T.);
#6296=ORIENTED_EDGE('',*,*,#4779,.T.);
#6297=ORIENTED_EDGE('',*,*,#4780,.T.);
#6298=ORIENTED_EDGE('',*,*,#4781,.T.);
#6299=ORIENTED_EDGE('',*,*,#4782,.F.);
#6300=ORIENTED_EDGE('',*,*,#4783,.T.);
#6301=ORIENTED_EDGE('',*,*,#4784,.T.);
#6302=ORIENTED_EDGE('',*,*,#4785,.T.);
#6303=ORIENTED_EDGE('',*,*,#4780,.F.);
#6304=ORIENTED_EDGE('',*,*,#4786,.T.);
#6305=ORIENTED_EDGE('',*,*,#4787,.T.);
#6306=ORIENTED_EDGE('',*,*,#4788,.T.);
#6307=ORIENTED_EDGE('',*,*,#4784,.F.);
#6308=ORIENTED_EDGE('',*,*,#4789,.T.);
#6309=ORIENTED_EDGE('',*,*,#4790,.T.);
#6310=ORIENTED_EDGE('',*,*,#4791,.T.);
#6311=ORIENTED_EDGE('',*,*,#4787,.F.);
#6312=ORIENTED_EDGE('',*,*,#4792,.T.);
#6313=ORIENTED_EDGE('',*,*,#4793,.T.);
#6314=ORIENTED_EDGE('',*,*,#4794,.T.);
#6315=ORIENTED_EDGE('',*,*,#4790,.F.);
#6316=ORIENTED_EDGE('',*,*,#4795,.T.);
#6317=ORIENTED_EDGE('',*,*,#4782,.T.);
#6318=ORIENTED_EDGE('',*,*,#4796,.T.);
#6319=ORIENTED_EDGE('',*,*,#4793,.F.);
#6320=ORIENTED_EDGE('',*,*,#4795,.F.);
#6321=ORIENTED_EDGE('',*,*,#4792,.F.);
#6322=ORIENTED_EDGE('',*,*,#4789,.F.);
#6323=ORIENTED_EDGE('',*,*,#4786,.F.);
#6324=ORIENTED_EDGE('',*,*,#4783,.F.);
#6325=ORIENTED_EDGE('',*,*,#4779,.F.);
#6326=ORIENTED_EDGE('',*,*,#4796,.F.);
#6327=ORIENTED_EDGE('',*,*,#4781,.F.);
#6328=ORIENTED_EDGE('',*,*,#4785,.F.);
#6329=ORIENTED_EDGE('',*,*,#4788,.F.);
#6330=ORIENTED_EDGE('',*,*,#4791,.F.);
#6331=ORIENTED_EDGE('',*,*,#4794,.F.);
#6332=ORIENTED_EDGE('',*,*,#4797,.F.);
#6333=ORIENTED_EDGE('',*,*,#4798,.F.);
#6334=ORIENTED_EDGE('',*,*,#4799,.F.);
#6335=ORIENTED_EDGE('',*,*,#4800,.T.);
#6336=ORIENTED_EDGE('',*,*,#4798,.T.);
#6337=ORIENTED_EDGE('',*,*,#4800,.F.);
#6338=ORIENTED_EDGE('',*,*,#4801,.F.);
#6339=ORIENTED_EDGE('',*,*,#4802,.T.);
#6340=ORIENTED_EDGE('',*,*,#4799,.T.);
#6341=ORIENTED_EDGE('',*,*,#4802,.F.);
#6342=ORIENTED_EDGE('',*,*,#4803,.F.);
#6343=ORIENTED_EDGE('',*,*,#4804,.T.);
#6344=ORIENTED_EDGE('',*,*,#4801,.T.);
#6345=ORIENTED_EDGE('',*,*,#4804,.F.);
#6346=ORIENTED_EDGE('',*,*,#4803,.T.);
#6347=ORIENTED_EDGE('',*,*,#4805,.F.);
#6348=ORIENTED_EDGE('',*,*,#4806,.F.);
#6349=ORIENTED_EDGE('',*,*,#4807,.T.);
#6350=ORIENTED_EDGE('',*,*,#4805,.T.);
#6351=ORIENTED_EDGE('',*,*,#4807,.F.);
#6352=ORIENTED_EDGE('',*,*,#4797,.T.);
#6353=ORIENTED_EDGE('',*,*,#4808,.T.);
#6354=ORIENTED_EDGE('',*,*,#4806,.T.);
#6355=ORIENTED_EDGE('',*,*,#4808,.F.);
#6860=CYLINDRICAL_SURFACE('',#8655,0.35);
#6861=CYLINDRICAL_SURFACE('',#8663,0.1954);
#7216=ADVANCED_FACE('',(#1511),#1144,.F.);
#7217=ADVANCED_FACE('',(#1512),#1145,.F.);
#7218=ADVANCED_FACE('',(#1513),#1146,.F.);
#7219=ADVANCED_FACE('',(#1514),#1147,.F.);
#7220=ADVANCED_FACE('',(#1515),#1148,.F.);
#7221=ADVANCED_FACE('',(#1516),#1149,.F.);
#7222=ADVANCED_FACE('',(#1517),#1150,.F.);
#7223=ADVANCED_FACE('',(#1518),#1151,.F.);
#7224=ADVANCED_FACE('',(#1519),#1152,.F.);
#7225=ADVANCED_FACE('',(#1520),#1153,.T.);
#7226=ADVANCED_FACE('',(#1521),#484,.T.);
#7227=ADVANCED_FACE('',(#1522),#6860,.T.);
#7228=ADVANCED_FACE('',(#1523),#485,.T.);
#7229=ADVANCED_FACE('',(#1524,#946),#1154,.T.);
#7230=ADVANCED_FACE('',(#1525),#486,.T.);
#7231=ADVANCED_FACE('',(#1526),#6861,.T.);
#7372=CLOSED_SHELL('',(#7216,#7217,#7218,#7219,#7220,#7221,#7222,#7223));
#7373=CLOSED_SHELL('',(#7224,#7225,#7226,#7227,#7228,#7229,#7230,#7231));
#8640=AXIS2_PLACEMENT_3D('',#13822,#10658,#10659);
#8641=AXIS2_PLACEMENT_3D('',#13823,#10660,#10661);
#8642=AXIS2_PLACEMENT_3D('',#13832,#10666,#10667);
#8643=AXIS2_PLACEMENT_3D('',#13838,#10671,#10672);
#8644=AXIS2_PLACEMENT_3D('',#13844,#10676,#10677);
#8645=AXIS2_PLACEMENT_3D('',#13850,#10681,#10682);
#8646=AXIS2_PLACEMENT_3D('',#13856,#10686,#10687);
#8647=AXIS2_PLACEMENT_3D('',#13859,#10690,#10691);
#8648=AXIS2_PLACEMENT_3D('',#13860,#10692,#10693);
#8649=AXIS2_PLACEMENT_3D('',#13861,#10694,#10695);
#8650=AXIS2_PLACEMENT_3D('',#13863,#10696,#10697);
#8651=AXIS2_PLACEMENT_3D('',#13864,#10698,#10699);
#8652=AXIS2_PLACEMENT_3D('',#13866,#10700,#10701);
#8653=AXIS2_PLACEMENT_3D('',#13867,#10702,#10703);
#8654=AXIS2_PLACEMENT_3D('',#13869,#10704,#10705);
#8655=AXIS2_PLACEMENT_3D('',#13871,#10707,#10708);
#8656=AXIS2_PLACEMENT_3D('',#13873,#10709,#10710);
#8657=AXIS2_PLACEMENT_3D('',#13875,#10712,#10713);
#8658=AXIS2_PLACEMENT_3D('',#13877,#10714,#10715);
#8659=AXIS2_PLACEMENT_3D('',#13879,#10717,#10718);
#8660=AXIS2_PLACEMENT_3D('',#13881,#10719,#10720);
#8661=AXIS2_PLACEMENT_3D('',#13882,#10721,#10722);
#8662=AXIS2_PLACEMENT_3D('',#13884,#10723,#10724);
#8663=AXIS2_PLACEMENT_3D('',#13886,#10726,#10727);
#10658=DIRECTION('axis',(0.,0.,1.));
#10659=DIRECTION('refdir',(1.,0.,0.));
#10660=DIRECTION('center_axis',(0.866025403784439,0.,-0.5));
#10661=DIRECTION('ref_axis',(0.5,0.,0.866025403784439));
#10662=DIRECTION('',(-0.5,0.,-0.866025403784439));
#10663=DIRECTION('',(0.,-1.,0.));
#10664=DIRECTION('',(0.5,0.,0.866025403784439));
#10665=DIRECTION('',(0.,-1.,0.));
#10666=DIRECTION('center_axis',(1.60246890531964E-16,0.,-1.));
#10667=DIRECTION('ref_axis',(1.,0.,1.60246890531964E-16));
#10668=DIRECTION('',(-1.,0.,-1.60246890531964E-16));
#10669=DIRECTION('',(0.,-1.,0.));
#10670=DIRECTION('',(1.,0.,1.60246890531964E-16));
#10671=DIRECTION('center_axis',(-0.866025403784439,0.,-0.5));
#10672=DIRECTION('ref_axis',(0.5,0.,-0.866025403784439));
#10673=DIRECTION('',(-0.5,0.,0.866025403784439));
#10674=DIRECTION('',(0.,-1.,0.));
#10675=DIRECTION('',(0.5,0.,-0.866025403784439));
#10676=DIRECTION('center_axis',(-0.866025403784439,0.,0.5));
#10677=DIRECTION('ref_axis',(-0.5,0.,-0.866025403784439));
#10678=DIRECTION('',(0.5,0.,0.866025403784439));
#10679=DIRECTION('',(0.,-1.,0.));
#10680=DIRECTION('',(-0.5,0.,-0.866025403784439));
#10681=DIRECTION('center_axis',(-1.60246890531964E-16,0.,1.));
#10682=DIRECTION('ref_axis',(-1.,0.,-1.60246890531964E-16));
#10683=DIRECTION('',(1.,0.,1.60246890531964E-16));
#10684=DIRECTION('',(0.,-1.,0.));
#10685=DIRECTION('',(-1.,0.,-1.60246890531964E-16));
#10686=DIRECTION('center_axis',(0.866025403784439,0.,0.5));
#10687=DIRECTION('ref_axis',(-0.5,0.,0.866025403784439));
#10688=DIRECTION('',(0.5,0.,-0.866025403784439));
#10689=DIRECTION('',(-0.5,0.,0.866025403784439));
#10690=DIRECTION('center_axis',(0.,1.,0.));
#10691=DIRECTION('ref_axis',(1.,0.,0.));
#10692=DIRECTION('center_axis',(0.,-1.,0.));
#10693=DIRECTION('ref_axis',(0.,0.,-1.));
#10694=DIRECTION('center_axis',(0.,1.,0.));
#10695=DIRECTION('ref_axis',(1.,0.,0.));
#10696=DIRECTION('center_axis',(0.,1.,0.));
#10697=DIRECTION('ref_axis',(1.,0.,0.));
#10698=DIRECTION('center_axis',(0.,1.,0.));
#10699=DIRECTION('ref_axis',(0.,0.,1.));
#10700=DIRECTION('center_axis',(0.,-1.,0.));
#10701=DIRECTION('ref_axis',(1.,0.,0.));
#10702=DIRECTION('center_axis',(0.,-1.,0.));
#10703=DIRECTION('ref_axis',(1.,0.,0.));
#10704=DIRECTION('center_axis',(0.,-1.,0.));
#10705=DIRECTION('ref_axis',(1.,0.,0.));
#10706=DIRECTION('',(0.707106781186547,0.707106781186548,8.65956056235493E-17));
#10707=DIRECTION('center_axis',(0.,-1.,0.));
#10708=DIRECTION('ref_axis',(1.,0.,0.));
#10709=DIRECTION('center_axis',(0.,-1.,0.));
#10710=DIRECTION('ref_axis',(1.,0.,0.));
#10711=DIRECTION('',(0.,1.,0.));
#10712=DIRECTION('center_axis',(0.,1.,0.));
#10713=DIRECTION('ref_axis',(1.,0.,0.));
#10714=DIRECTION('center_axis',(0.,-1.,0.));
#10715=DIRECTION('ref_axis',(1.,0.,0.));
#10716=DIRECTION('',(-0.707106781186547,0.707106781186548,-8.65956056235493E-17));
#10717=DIRECTION('center_axis',(0.,-1.,0.));
#10718=DIRECTION('ref_axis',(0.,0.,-1.));
#10719=DIRECTION('center_axis',(0.,-1.,0.));
#10720=DIRECTION('ref_axis',(1.,0.,0.));
#10721=DIRECTION('center_axis',(0.,1.,0.));
#10722=DIRECTION('ref_axis',(1.,0.,0.));
#10723=DIRECTION('center_axis',(0.,1.,0.));
#10724=DIRECTION('ref_axis',(1.,0.,0.));
#10725=DIRECTION('',(-0.447213595499958,0.894427190999916,-5.47678698264203E-17));
#10726=DIRECTION('center_axis',(0.,-1.,0.));
#10727=DIRECTION('ref_axis',(1.,0.,0.));
#10728=DIRECTION('',(0.,1.,0.));
#13822=CARTESIAN_POINT('',(0.,0.,0.));
#13823=CARTESIAN_POINT('Origin',(0.0866025403784439,-0.4,-0.15));
#13824=CARTESIAN_POINT('',(0.173205080756888,-0.4,0.));
#13825=CARTESIAN_POINT('',(0.0866025403784439,-0.4,-0.15));
#13826=CARTESIAN_POINT('',(0.173205080756888,-0.4,0.));
#13827=CARTESIAN_POINT('',(0.0866025403784439,-0.64,-0.15));
#13828=CARTESIAN_POINT('',(0.0866025403784439,-0.4,-0.15));
#13829=CARTESIAN_POINT('',(0.173205080756888,-0.64,0.));
#13830=CARTESIAN_POINT('',(0.173205080756888,-0.64,0.));
#13831=CARTESIAN_POINT('',(0.173205080756888,-0.4,0.));
#13832=CARTESIAN_POINT('Origin',(-0.0866025403784438,-0.4,-0.15));
#13833=CARTESIAN_POINT('',(-0.0866025403784438,-0.4,-0.15));
#13834=CARTESIAN_POINT('',(0.0866025403784439,-0.4,-0.15));
#13835=CARTESIAN_POINT('',(-0.0866025403784438,-0.64,-0.15));
#13836=CARTESIAN_POINT('',(-0.0866025403784438,-0.4,-0.15));
#13837=CARTESIAN_POINT('',(0.0866025403784439,-0.64,-0.15));
#13838=CARTESIAN_POINT('Origin',(-0.173205080756888,-0.4,-2.77555756156289E-17));
#13839=CARTESIAN_POINT('',(-0.173205080756888,-0.4,-2.12115047744981E-17));
#13840=CARTESIAN_POINT('',(-0.0866025403784438,-0.4,-0.15));
#13841=CARTESIAN_POINT('',(-0.173205080756888,-0.64,-2.77555756156289E-17));
#13842=CARTESIAN_POINT('',(-0.173205080756888,-0.4,-2.12115047744981E-17));
#13843=CARTESIAN_POINT('',(-0.0866025403784438,-0.64,-0.15));
#13844=CARTESIAN_POINT('Origin',(-0.0866025403784439,-0.4,0.15));
#13845=CARTESIAN_POINT('',(-0.0866025403784439,-0.4,0.15));
#13846=CARTESIAN_POINT('',(-0.173205080756888,-0.4,-2.12115047744981E-17));
#13847=CARTESIAN_POINT('',(-0.0866025403784439,-0.64,0.15));
#13848=CARTESIAN_POINT('',(-0.0866025403784439,-0.4,0.15));
#13849=CARTESIAN_POINT('',(-0.173205080756888,-0.64,-2.12115047744981E-17));
#13850=CARTESIAN_POINT('Origin',(0.0866025403784439,-0.4,0.15));
#13851=CARTESIAN_POINT('',(0.0866025403784439,-0.4,0.15));
#13852=CARTESIAN_POINT('',(-0.0866025403784439,-0.4,0.15));
#13853=CARTESIAN_POINT('',(0.0866025403784439,-0.64,0.15));
#13854=CARTESIAN_POINT('',(0.0866025403784439,-0.4,0.15));
#13855=CARTESIAN_POINT('',(-0.0866025403784439,-0.64,0.15));
#13856=CARTESIAN_POINT('Origin',(0.173205080756888,-0.4,0.));
#13857=CARTESIAN_POINT('',(0.0866025403784439,-0.4,0.15));
#13858=CARTESIAN_POINT('',(0.0866025403784439,-0.64,0.15));
#13859=CARTESIAN_POINT('Origin',(0.,-0.4,-2.77555756156289E-17));
#13860=CARTESIAN_POINT('Origin',(0.,-0.64,-2.77555756156289E-17));
#13861=CARTESIAN_POINT('Origin',(0.,-1.,0.));
#13862=CARTESIAN_POINT('',(-0.1954,-1.,2.39295984553393E-17));
#13863=CARTESIAN_POINT('Origin',(0.,-1.,0.));
#13864=CARTESIAN_POINT('Origin',(0.3,0.4,0.));
#13865=CARTESIAN_POINT('',(-0.3,0.4,-3.67394039744206E-17));
#13866=CARTESIAN_POINT('Origin',(0.,0.4,0.));
#13867=CARTESIAN_POINT('Origin',(0.,0.375,0.));
#13868=CARTESIAN_POINT('',(-0.35,0.35,-4.28626379701573E-17));
#13869=CARTESIAN_POINT('Origin',(0.,0.35,0.));
#13870=CARTESIAN_POINT('',(-0.325,0.375,-3.9801020972289E-17));
#13871=CARTESIAN_POINT('Origin',(0.,0.19,0.));
#13872=CARTESIAN_POINT('',(-0.35,0.03,-4.28626379701574E-17));
#13873=CARTESIAN_POINT('Origin',(0.,0.03,0.));
#13874=CARTESIAN_POINT('',(-0.35,0.19,-4.28626379701574E-17));
#13875=CARTESIAN_POINT('Origin',(0.,0.0149999999999999,0.));
#13876=CARTESIAN_POINT('',(-0.32,-3.29597460435593E-17,-3.91886975727153E-17));
#13877=CARTESIAN_POINT('Origin',(0.,0.,0.));
#13878=CARTESIAN_POINT('',(-0.335,0.0149999999999999,-4.10256677714363E-17));
#13879=CARTESIAN_POINT('Origin',(0.22,0.,0.));
#13880=CARTESIAN_POINT('',(-0.22,-6.93889390390723E-18,-2.69422295812418E-17));
#13881=CARTESIAN_POINT('Origin',(0.,0.,0.));
#13882=CARTESIAN_POINT('Origin',(0.,-0.02,0.));
#13883=CARTESIAN_POINT('',(-0.1954,-0.0492,2.39295984553393E-17));
#13884=CARTESIAN_POINT('Origin',(0.,-0.0492,0.));
#13885=CARTESIAN_POINT('',(-0.21,-0.02,-2.57175827820944E-17));
#13886=CARTESIAN_POINT('Origin',(0.,-0.8,0.));
#13887=CARTESIAN_POINT('',(-0.1954,-0.8,-2.39295984553393E-17));
#14441=UNCERTAINTY_MEASURE_WITH_UNIT(LENGTH_MEASURE(0.001),#14513,
'DISTANCE_ACCURACY_VALUE',
'Maximum model space distance between geometric entities at asserted c
onnectivities');
#14455=UNCERTAINTY_MEASURE_WITH_UNIT(LENGTH_MEASURE(0.001),#14513,
'DISTANCE_ACCURACY_VALUE',
'Maximum model space distance between geometric entities at asserted c
onnectivities');
#14498=(
GEOMETRIC_REPRESENTATION_CONTEXT(3)
GLOBAL_UNCERTAINTY_ASSIGNED_CONTEXT((#14441))
GLOBAL_UNIT_ASSIGNED_CONTEXT((#14513,#14515,#14516))
REPRESENTATION_CONTEXT('','3D')
);
#14512=(
GEOMETRIC_REPRESENTATION_CONTEXT(3)
GLOBAL_UNCERTAINTY_ASSIGNED_CONTEXT((#14455))
GLOBAL_UNIT_ASSIGNED_CONTEXT((#14513,#14515,#14516))
REPRESENTATION_CONTEXT('','3D')
);
#14513=(
LENGTH_UNIT()
NAMED_UNIT(*)
SI_UNIT(.CENTI.,.METRE.)
);
#14515=(
NAMED_UNIT(*)
PLANE_ANGLE_UNIT()
SI_UNIT($,.RADIAN.)
);
#14516=(
NAMED_UNIT(*)
SI_UNIT($,.STERADIAN.)
SOLID_ANGLE_UNIT()
);
#14559=SHAPE_DEFINITION_REPRESENTATION(#14620,#14783);
#14620=PRODUCT_DEFINITION_SHAPE('',$,#14840);
#14783=SHAPE_REPRESENTATION('',(#8640),#14498);
#14797=PRODUCT_DEFINITION_CONTEXT('part definition',#14967,'design');
#14840=PRODUCT_DEFINITION('M4x10 Cap Screw','M4x10 Cap Screw',#14896,#14797);
#14896=PRODUCT_DEFINITION_FORMATION('',$,#15011);
#14967=APPLICATION_CONTEXT(
'Core Data for Automotive Mechanical Design Process');
#14968=PRODUCT_CONTEXT('part definition',#14967,'mechanical');
#15011=PRODUCT('M4x10 Cap Screw','M4x10 Cap Screw','M4x10 Cap Screw',(#14968));
#15088=COLOUR_RGB('Black',0.12,0.14,0.17);
#15089=FILL_AREA_STYLE_COLOUR('',#15088);
#15090=FILL_AREA_STYLE('',(#15089));
#15091=SURFACE_STYLE_FILL_AREA(#15090);
#15092=SURFACE_SIDE_STYLE('',(#15091));
#15093=SURFACE_STYLE_USAGE(.BOTH.,#15092);
#15094=PRESENTATION_STYLE_ASSIGNMENT((#15093));
ENDSEC;
END-ISO-10303-21;
